ISO-10303-21;
HEADER;
FILE_DESCRIPTION (('STEP AP203'),
    '1' );
FILE_NAME ('1602p_c_20.step',
    '2026-10-31T14:11:27',
    ( '' ),
    ( '' ),
    'SwSTEP 2.0',
    'SolidWorks 2024',
    '' );
FILE_SCHEMA (( 'AUTOMOTIVE_DESIGN' ));
ENDSEC;

DATA;
#198=ORIENTED_EDGE ( 'NONE', *, *, #5195, .T. ) ;
#239=PLANE ( 'NONE',  #21167 ) ;
#399=ORIENTED_EDGE ( 'NONE', *, *, #15334, .T. ) ;
#415=DIRECTION ( 'NONE',  ( 1.000000000000000000, 0.000000000000000000, 0.000000000000000000 ) ) ;
#465=EDGE_CURVE ( 'NONE', #2857, #7141, #671, .T. ) ;
#499=EDGE_CURVE ( 'NONE', #16530, #2857, #12789, .T. ) ;
#671=CIRCLE ( 'NONE', #7138, 2.499999999999998668 ) ;
#798=AXIS2_PLACEMENT_3D ( 'NONE', #9639, #22071, #14833 ) ;
#817=EDGE_CURVE ( 'NONE', #7141, #2857, #17822, .T. ) ;
#929=DIRECTION ( 'NONE',  ( -4.028143194477080210E-16, -2.054129435991050111E-15, -1.000000000000000000 ) ) ;
#1048=ORIENTED_EDGE ( 'NONE', *, *, #465, .F. ) ;
#1145=DIRECTION ( 'NONE',  ( 4.028143194477080210E-16, 2.054129435991050111E-15, 1.000000000000000000 ) ) ;
#1230=EDGE_LOOP ( 'NONE', ( #18458, #11550 ) ) ;
#1261=ORIENTED_EDGE ( 'NONE', *, *, #22734, .T. ) ;
#1349=MANIFOLD_SOLID_BREP ( 'Imported1', #19377 ) ;
#2045=DIRECTION ( 'NONE',  ( -4.028143194477080210E-16, -2.054129435991050111E-15, -1.000000000000000000 ) ) ;
#2135=EDGE_CURVE ( 'NONE', #22213, #9474, #3256, .T. ) ;
#2311=DIRECTION ( 'NONE',  ( -4.028143194477080210E-16, -2.054129435991050111E-15, -1.000000000000000000 ) ) ;
#2443=CARTESIAN_POINT ( 'NONE',  ( -20.00000000000000000, -20.00000000000000000, -4.999999999995470290 ) ) ;
#2569=CARTESIAN_POINT ( 'NONE',  ( 0.000000000000000000, 0.000000000000000000, 0.000000000000000000 ) ) ;
#2857=VERTEX_POINT ( 'NONE', #7286 ) ;
#3035=CIRCLE ( 'NONE', #4939, 5.000000000000000888 ) ;
#3140=ADVANCED_FACE ( 'NONE', ( #13994 ), #17572, .F. ) ;
#3147=AXIS2_PLACEMENT_3D ( 'NONE', #20459, #9427, #6088 ) ;
#3189=DIRECTION ( 'NONE',  ( 0.000000000000000000, -1.000000000000000000, 2.081668171172169697E-15 ) ) ;
#3256=CIRCLE ( 'NONE', #20326, 5.000000000000000888 ) ;
#3331=FACE_OUTER_BOUND ( 'NONE', #1230, .T. ) ;
#3400=CARTESIAN_POINT ( 'NONE',  ( -20.00000000000000000, -17.50000000000000000, -4.999999999995474731 ) ) ;
#3444=FACE_BOUND ( 'NONE', #9533, .T. ) ;
#3489=ORIENTED_EDGE ( 'NONE', *, *, #11916, .F. ) ;
#3710=ORIENTED_EDGE ( 'NONE', *, *, #12868, .F. ) ;
#4155=ORIENTED_EDGE ( 'NONE', *, *, #5195, .F. ) ;
#4500=ORIENTED_EDGE ( 'NONE', *, *, #817, .F. ) ;
#4561=VERTEX_POINT ( 'NONE', #7992 ) ;
#4837=DIRECTION ( 'NONE',  ( 0.000000000000000000, -1.000000000000000000, 2.081668171172169697E-15 ) ) ;
#4846=DIRECTION ( 'NONE',  ( -4.028143194477080210E-16, -2.054129435991050111E-15, -1.000000000000000000 ) ) ;
#4887=ORIENTED_EDGE ( 'NONE', *, *, #19403, .T. ) ;
#4939=AXIS2_PLACEMENT_3D ( 'NONE', #19474, #6528, #19349 ) ;
#5029=CARTESIAN_POINT ( 'NONE',  ( -20.00000000000000000, -15.00000000000000000, -4.999999999995480060 ) ) ;
#5120=DIRECTION ( 'NONE',  ( 8.274327508162393116E-31, 2.054129435991050111E-15, 1.000000000000000000 ) ) ;
#5195=EDGE_CURVE ( 'NONE', #4561, #21838, #3035, .T. ) ;
#5263=EDGE_LOOP ( 'NONE', ( #12585, #13550 ) ) ;
#5333=APPLICATION_CONTEXT ( 'configuration controlled 3d designs of mechanical parts and assemblies' ) ;
#5564=EDGE_CURVE ( 'NONE', #16530, #19340, #9454, .T. ) ;
#5567=AXIS2_PLACEMENT_3D ( 'NONE', #14349, #12239, #12117 ) ;
#6088=DIRECTION ( 'NONE',  ( 0.000000000000000000, -1.000000000000000000, 2.081668171172168119E-15 ) ) ;
#6284=DIRECTION ( 'NONE',  ( 0.000000000000000000, -1.000000000000000000, 2.081668171172169697E-15 ) ) ;
#6413=ORIENTED_EDGE ( 'NONE', *, *, #499, .F. ) ;
#6528=DIRECTION ( 'NONE',  ( 4.028143194477080210E-16, 2.054129435991050111E-15, 1.000000000000000000 ) ) ;
#6637=PRODUCT_DEFINITION ( 'UNKNOWN', '', #16369, #14206 ) ;
#6700=( LENGTH_UNIT ( ) NAMED_UNIT ( * ) SI_UNIT ( .MILLI., .METRE. ) );
#6739=CARTESIAN_POINT ( 'NONE',  ( -20.00000000000000000, -25.00000000000000000, -5.499999999995458744 ) ) ;
#6866=DIRECTION ( 'NONE',  ( -4.028143194477080210E-16, -2.054129435991050111E-15, -1.000000000000000000 ) ) ;
#7004=FACE_OUTER_BOUND ( 'NONE', #16361, .T. ) ;
#7138=AXIS2_PLACEMENT_3D ( 'NONE', #17431, #1145, #4837 ) ;
#7141=VERTEX_POINT ( 'NONE', #10301 ) ;
#7246=DIRECTION ( 'NONE',  ( -4.028143194477080210E-16, -2.054129435991050111E-15, -1.000000000000000000 ) ) ;
#7286=CARTESIAN_POINT ( 'NONE',  ( -20.00000000000000000, -17.50000000000000000, -5.499999999995474731 ) ) ;
#7514=CARTESIAN_POINT ( 'NONE',  ( -20.00000000000000000, -20.00000000000000000, -5.499999999995469402 ) ) ;
#7788=DIRECTION ( 'NONE',  ( -4.028143194477080210E-16, -2.054129435991050111E-15, -1.000000000000000000 ) ) ;
#7916=DIRECTION ( 'NONE',  ( 4.028143194477080210E-16, 2.054129435991050111E-15, 1.000000000000000000 ) ) ;
#7992=CARTESIAN_POINT ( 'NONE',  ( -20.00000000000000000, -15.00000000000000000, -5.499999999995480060 ) ) ;
#8242=( NAMED_UNIT ( * ) SI_UNIT ( $, .STERADIAN. ) SOLID_ANGLE_UNIT ( ) );
#8331=ORIENTED_EDGE ( 'NONE', *, *, #12868, .T. ) ;
#8339=ADVANCED_FACE ( 'NONE', ( #7004 ), #19460, .F. ) ;
#8665=AXIS2_PLACEMENT_3D ( 'NONE', #18853, #7916, #9949 ) ;
#8673=ORIENTED_EDGE ( 'NONE', *, *, #5564, .F. ) ;
#8677=VECTOR ( 'NONE', #18194, 1000.000000000000000 ) ;
#8679=DIRECTION ( 'NONE',  ( 0.000000000000000000, -1.000000000000000000, 2.081668171172168119E-15 ) ) ;
#8849=ORIENTED_EDGE ( 'NONE', *, *, #5564, .T. ) ;
#9137=LINE ( 'NONE', #15827, #20389 ) ;
#9381=FACE_OUTER_BOUND ( 'NONE', #16692, .T. ) ;
#9427=DIRECTION ( 'NONE',  ( 4.028143194477080210E-16, 2.054129435991050111E-15, 1.000000000000000000 ) ) ;
#9439=EDGE_CURVE ( 'NONE', #19340, #7141, #12746, .T. ) ;
#9454=CIRCLE ( 'NONE', #17792, 2.499999999999998668 ) ;
#9474=VERTEX_POINT ( 'NONE', #12514 ) ;
#9533=EDGE_LOOP ( 'NONE', ( #399, #8849 ) ) ;
#9639=CARTESIAN_POINT ( 'NONE',  ( -20.00000000000000000, -20.00000000000000000, -4.999999999995470290 ) ) ;
#9949=DIRECTION ( 'NONE',  ( 0.000000000000000000, -1.000000000000000000, 2.081668171172168119E-15 ) ) ;
#10191=CIRCLE ( 'NONE', #8665, 5.000000000000000888 ) ;
#10229=ORIENTED_EDGE ( 'NONE', *, *, #9439, .F. ) ;
#10301=CARTESIAN_POINT ( 'NONE',  ( -20.00000000000000000, -22.50000000000000000, -5.499999999995464073 ) ) ;
#10879=ORIENTED_EDGE ( 'NONE', *, *, #499, .T. ) ;
#10951=DIRECTION ( 'NONE',  ( 1.000000000000000000, -4.028143194477080210E-16, -1.401298464324815982E-46 ) ) ;
#11549=CYLINDRICAL_SURFACE ( 'NONE', #798, 5.000000000000000888 ) ;
#11550=ORIENTED_EDGE ( 'NONE', *, *, #2135, .T. ) ;
#11890=APPLICATION_CONTEXT ( 'configuration controlled 3d designs of mechanical parts and assemblies' ) ;
#11897=ORIENTED_EDGE ( 'NONE', *, *, #15334, .F. ) ;
#11916=EDGE_CURVE ( 'NONE', #9474, #22213, #10191, .T. ) ;
#11930=EDGE_LOOP ( 'NONE', ( #8673, #10879, #4500, #10229 ) ) ;
#12018=ORIENTED_EDGE ( 'NONE', *, *, #22734, .F. ) ;
#12072=EDGE_LOOP ( 'NONE', ( #22925, #4155 ) ) ;
#12117=DIRECTION ( 'NONE',  ( 0.000000000000000000, -1.000000000000000000, 2.081668171172169697E-15 ) ) ;
#12239=DIRECTION ( 'NONE',  ( -4.028143194477080210E-16, -2.054129435991050111E-15, -1.000000000000000000 ) ) ;
#12514=CARTESIAN_POINT ( 'NONE',  ( -20.00000000000000000, -25.00000000000000000, -4.999999999995459632 ) ) ;
#12585=ORIENTED_EDGE ( 'NONE', *, *, #817, .T. ) ;
#12739=AXIS2_PLACEMENT_3D ( 'NONE', #2569, #13380, #415 ) ;
#12746=LINE ( 'NONE', #14636, #19357 ) ;
#12780=ADVANCED_BREP_SHAPE_REPRESENTATION ( '', ( #1349, #12739 ), #21837 ) ;
#12789=LINE ( 'NONE', #3400, #22284 ) ;
#12868=EDGE_CURVE ( 'NONE', #22213, #4561, #17739, .T. ) ;
#12963=ADVANCED_FACE ( 'NONE', ( #18324, #21972 ), #239, .F. ) ;
#13052=AXIS2_PLACEMENT_3D ( 'NONE', #14227, #4846, #3189 ) ;
#13380=DIRECTION ( 'NONE',  ( 0.000000000000000000, 0.000000000000000000, 1.000000000000000000 ) ) ;
#13550=ORIENTED_EDGE ( 'NONE', *, *, #465, .T. ) ;
#13578=SHAPE_REPRESENTATION_RELATIONSHIP ( 'NONE' , 'NONE' ,  #16866, #12780 ) ;
#13602=CARTESIAN_POINT ( 'NONE',  ( -20.00000000000000000, -20.00000000000000000, -5.499999999995469402 ) ) ;
#13806=DIRECTION ( 'NONE',  ( 0.000000000000000000, -1.000000000000000000, 2.081668171172168119E-15 ) ) ;
#13994=FACE_OUTER_BOUND ( 'NONE', #11930, .T. ) ;
#14206=DESIGN_CONTEXT ( 'detailed design', #5333, 'design' ) ;
#14223=PRODUCT ( '1602p_c_20', '1602p_c_20', '', ( #18578 ) ) ;
#14227=CARTESIAN_POINT ( 'NONE',  ( -20.00000000000000000, -20.00000000000000000, -4.999999999995470290 ) ) ;
#14252=PLANE ( 'NONE',  #20004 ) ;
#14349=CARTESIAN_POINT ( 'NONE',  ( -20.00000000000000000, -20.00000000000000000, -4.999999999995470290 ) ) ;
#14636=CARTESIAN_POINT ( 'NONE',  ( -20.00000000000000000, -22.50000000000000000, -4.999999999995464961 ) ) ;
#14833=DIRECTION ( 'NONE',  ( 0.000000000000000000, -1.000000000000000000, 2.081668171172168119E-15 ) ) ;
#14941=ADVANCED_FACE ( 'NONE', ( #3444, #3331 ), #14252, .T. ) ;
#15150=ADVANCED_FACE ( 'NONE', ( #9381 ), #11549, .T. ) ;
#15225=ORIENTED_EDGE ( 'NONE', *, *, #9439, .T. ) ;
#15242=( NAMED_UNIT ( * ) PLANE_ANGLE_UNIT ( ) SI_UNIT ( $, .RADIAN. ) );
#15258=DIRECTION ( 'NONE',  ( 0.000000000000000000, -1.000000000000000000, 2.081668171172169697E-15 ) ) ;
#15334=EDGE_CURVE ( 'NONE', #19340, #16530, #16742, .T. ) ;
#15827=CARTESIAN_POINT ( 'NONE',  ( -20.00000000000000000, -25.00000000000000000, -4.999999999995459632 ) ) ;
#15916=CARTESIAN_POINT ( 'NONE',  ( -20.00000000000000000, -20.00000000000000000, -4.999999999995470290 ) ) ;
#16040=CIRCLE ( 'NONE', #3147, 5.000000000000000888 ) ;
#16361=EDGE_LOOP ( 'NONE', ( #6413, #11897, #15225, #1048 ) ) ;
#16369=PRODUCT_DEFINITION_FORMATION_WITH_SPECIFIED_SOURCE ( 'ANY', '', #14223, .NOT_KNOWN. ) ;
#16530=VERTEX_POINT ( 'NONE', #18784 ) ;
#16642=CARTESIAN_POINT ( 'NONE',  ( -20.00000000000000000, -22.50000000000000000, -4.999999999995464961 ) ) ;
#16692=EDGE_LOOP ( 'NONE', ( #22624, #8331, #198, #12018 ) ) ;
#16742=CIRCLE ( 'NONE', #18271, 2.499999999999998668 ) ;
#16751=DIRECTION ( 'NONE',  ( 1.000000000000000000, -4.028143194477080210E-16, -1.401298464324815982E-46 ) ) ;
#16866=SHAPE_REPRESENTATION ( '1602p_c_20', ( #12739 ), #21837 ) ;
#17134=SHAPE_DEFINITION_REPRESENTATION ( #23105, #16866 ) ;
#17246=ADVANCED_FACE ( 'NONE', ( #20477 ), #22245, .T. ) ;
#17287=CARTESIAN_POINT ( 'NONE',  ( -20.00000000000000000, -20.00000000000000000, -4.999999999995470290 ) ) ;
#17431=CARTESIAN_POINT ( 'NONE',  ( -20.00000000000000000, -20.00000000000000000, -5.499999999995469402 ) ) ;
#17572=CYLINDRICAL_SURFACE ( 'NONE', #5567, 2.499999999999998668 ) ;
#17739=LINE ( 'NONE', #5029, #8677 ) ;
#17792=AXIS2_PLACEMENT_3D ( 'NONE', #17287, #7788, #15258 ) ;
#17816=CARTESIAN_POINT ( 'NONE',  ( -20.00000000000000000, -20.00000000000000000, -4.999999999995470290 ) ) ;
#17822=CIRCLE ( 'NONE', #18594, 2.499999999999998668 ) ;
#18194=DIRECTION ( 'NONE',  ( -4.028143194477080210E-16, -2.054129435991050111E-15, -1.000000000000000000 ) ) ;
#18271=AXIS2_PLACEMENT_3D ( 'NONE', #19126, #929, #6284 ) ;
#18324=FACE_BOUND ( 'NONE', #5263, .T. ) ;
#18458=ORIENTED_EDGE ( 'NONE', *, *, #11916, .T. ) ;
#18578=MECHANICAL_CONTEXT ( 'NONE', #11890, 'mechanical' ) ;
#18594=AXIS2_PLACEMENT_3D ( 'NONE', #13602, #20725, #19077 ) ;
#18784=CARTESIAN_POINT ( 'NONE',  ( -20.00000000000000000, -17.50000000000000000, -4.999999999995474731 ) ) ;
#18849=CARTESIAN_POINT ( 'NONE',  ( -20.00000000000000000, -15.00000000000000000, -4.999999999995480060 ) ) ;
#18853=CARTESIAN_POINT ( 'NONE',  ( -20.00000000000000000, -20.00000000000000000, -4.999999999995470290 ) ) ;
#18998=EDGE_LOOP ( 'NONE', ( #3710, #3489, #1261, #4887 ) ) ;
#19077=DIRECTION ( 'NONE',  ( 0.000000000000000000, -1.000000000000000000, 2.081668171172169697E-15 ) ) ;
#19126=CARTESIAN_POINT ( 'NONE',  ( -20.00000000000000000, -20.00000000000000000, -4.999999999995470290 ) ) ;
#19244=DIRECTION ( 'NONE',  ( 4.028143194477080210E-16, 2.054129435991050111E-15, 1.000000000000000000 ) ) ;
#19340=VERTEX_POINT ( 'NONE', #16642 ) ;
#19349=DIRECTION ( 'NONE',  ( 0.000000000000000000, -1.000000000000000000, 2.081668171172168119E-15 ) ) ;
#19357=VECTOR ( 'NONE', #2045, 1000.000000000000000 ) ;
#19377=CLOSED_SHELL ( 'NONE', ( #15150, #3140, #8339, #17246, #12963, #14941 ) ) ;
#19403=EDGE_CURVE ( 'NONE', #21838, #4561, #16040, .T. ) ;
#19460=CYLINDRICAL_SURFACE ( 'NONE', #13052, 2.499999999999998668 ) ;
#19474=CARTESIAN_POINT ( 'NONE',  ( -20.00000000000000000, -20.00000000000000000, -5.499999999995469402 ) ) ;
#19475=AXIS2_PLACEMENT_3D ( 'NONE', #2443, #2311, #13806 ) ;
#19638=UNCERTAINTY_MEASURE_WITH_UNIT (LENGTH_MEASURE( 1.000000000000000082E-05 ), #6700, 'distance_accuracy_value', 'NONE');
#20004=AXIS2_PLACEMENT_3D ( 'NONE', #15916, #5120, #10951 ) ;
#20326=AXIS2_PLACEMENT_3D ( 'NONE', #17816, #19244, #8679 ) ;
#20389=VECTOR ( 'NONE', #7246, 1000.000000000000000 ) ;
#20459=CARTESIAN_POINT ( 'NONE',  ( -20.00000000000000000, -20.00000000000000000, -5.499999999995469402 ) ) ;
#20477=FACE_OUTER_BOUND ( 'NONE', #18998, .T. ) ;
#20725=DIRECTION ( 'NONE',  ( 4.028143194477080210E-16, 2.054129435991050111E-15, 1.000000000000000000 ) ) ;
#21167=AXIS2_PLACEMENT_3D ( 'NONE', #7514, #22211, #16751 ) ;
#21837=( GEOMETRIC_REPRESENTATION_CONTEXT ( 3 ) GLOBAL_UNCERTAINTY_ASSIGNED_CONTEXT ( ( #19638 ) ) GLOBAL_UNIT_ASSIGNED_CONTEXT ( ( #6700, #15242, #8242 ) ) REPRESENTATION_CONTEXT ( 'NONE', 'WORKASPACE' ) );
#21838=VERTEX_POINT ( 'NONE', #6739 ) ;
#21972=FACE_OUTER_BOUND ( 'NONE', #12072, .T. ) ;
#22071=DIRECTION ( 'NONE',  ( -4.028143194477080210E-16, -2.054129435991050111E-15, -1.000000000000000000 ) ) ;
#22211=DIRECTION ( 'NONE',  ( 8.274327508162393116E-31, 2.054129435991050111E-15, 1.000000000000000000 ) ) ;
#22213=VERTEX_POINT ( 'NONE', #18849 ) ;
#22245=CYLINDRICAL_SURFACE ( 'NONE', #19475, 5.000000000000000888 ) ;
#22284=VECTOR ( 'NONE', #6866, 1000.000000000000000 ) ;
#22624=ORIENTED_EDGE ( 'NONE', *, *, #2135, .F. ) ;
#22734=EDGE_CURVE ( 'NONE', #9474, #21838, #9137, .T. ) ;
#22925=ORIENTED_EDGE ( 'NONE', *, *, #19403, .F. ) ;
#23105=PRODUCT_DEFINITION_SHAPE ( 'NONE', 'NONE',  #6637 ) ;
#23536=COLOUR_RGB('Slate Gray', 0.40784314, 0.44705882, 0.49803922);
#23537=FILL_AREA_STYLE_COLOUR('',#23536);
#23538=FILL_AREA_STYLE('',(#23537));
#23539=SURFACE_STYLE_FILL_AREA(#23538);
#23540=SURFACE_SIDE_STYLE('',(#23539));
#23541=SURFACE_STYLE_USAGE(.BOTH.,#23540);
#23542=PRESENTATION_STYLE_ASSIGNMENT((#23541));
#23595=STYLED_ITEM('',(#23542),#1349);
#23596=MECHANICAL_DESIGN_GEOMETRIC_PRESENTATION_REPRESENTATION('',(#23595),#21837);
ENDSEC;
END-ISO-10303-21;
